ISO-10303-21;
HEADER;
/* Generated by software containing ST-Developer
 * from STEP Tools, Inc. (www.steptools.com) 
 */

FILE_DESCRIPTION(
/* description */ (''),
/* implementation_level */ '2;1');

FILE_NAME(
/* name */ 'Screw_01.step',
/* time_stamp */ '2026-10-04T22:47:03-07:00',
/* author */ (''),
/* organization */ (''),
/* preprocessor_version */ 'ST-DEVELOPER v20.2',
/* originating_system */ 'Autodesk Translation Framework v15.15.0.0',
/* authorisation */ '');

FILE_SCHEMA (('AUTOMOTIVE_DESIGN { 1 0 10303 214 3 1 1 }'));
ENDSEC;

DATA;
#10=MECHANICAL_DESIGN_GEOMETRIC_PRESENTATION_REPRESENTATION('',(#79),#19878);
#44=TOROIDAL_SURFACE('',#5228,8.911,1.);
#59=CONICAL_SURFACE('',#5225,7.28,0.832981266674429);
#60=CONICAL_SURFACE('',#5232,11.24,0.785398163397495);
#65=SHAPE_REPRESENTATION_RELATIONSHIP('SRR','None',#19909,#72);
#72=ADVANCED_BREP_SHAPE_REPRESENTATION('',(#86),#19873);
#79=STYLED_ITEM('',(#19952),#86);
#86=MANIFOLD_SOLID_BREP('Body1',#4827);
#94=FACE_BOUND('',#803,.T.);
#287=PLANE('',#5235);
#288=PLANE('',#5236);
#289=PLANE('',#5237);
#290=PLANE('',#5238);
#291=PLANE('',#5239);
#292=PLANE('',#5240);
#293=PLANE('',#5241);
#294=PLANE('',#5242);
#295=PLANE('',#5243);
#296=PLANE('',#5244);
#297=PLANE('',#5245);
#298=PLANE('',#5246);
#299=PLANE('',#5247);
#300=PLANE('',#5250);
#507=FACE_OUTER_BOUND('',#786,.T.);
#508=FACE_OUTER_BOUND('',#787,.T.);
#509=FACE_OUTER_BOUND('',#788,.T.);
#510=FACE_OUTER_BOUND('',#789,.T.);
#511=FACE_OUTER_BOUND('',#790,.T.);
#512=FACE_OUTER_BOUND('',#791,.T.);
#513=FACE_OUTER_BOUND('',#792,.T.);
#514=FACE_OUTER_BOUND('',#793,.T.);
#515=FACE_OUTER_BOUND('',#794,.T.);
#516=FACE_OUTER_BOUND('',#795,.T.);
#517=FACE_OUTER_BOUND('',#796,.T.);
#518=FACE_OUTER_BOUND('',#797,.T.);
#519=FACE_OUTER_BOUND('',#798,.T.);
#520=FACE_OUTER_BOUND('',#799,.T.);
#521=FACE_OUTER_BOUND('',#800,.T.);
#522=FACE_OUTER_BOUND('',#801,.T.);
#523=FACE_OUTER_BOUND('',#802,.T.);
#524=FACE_OUTER_BOUND('',#804,.T.);
#525=FACE_OUTER_BOUND('',#805,.T.);
#786=EDGE_LOOP('',(#4063,#4064,#4065,#4066));
#787=EDGE_LOOP('',(#4067,#4068,#4069,#4070));
#788=EDGE_LOOP('',(#4071,#4072,#4073,#4074));
#789=EDGE_LOOP('',(#4075,#4076,#4077,#4078));
#790=EDGE_LOOP('',(#4079,#4080,#4081));
#791=EDGE_LOOP('',(#4082,#4083,#4084));
#792=EDGE_LOOP('',(#4085,#4086,#4087));
#793=EDGE_LOOP('',(#4088,#4089,#4090));
#794=EDGE_LOOP('',(#4091,#4092,#4093));
#795=EDGE_LOOP('',(#4094,#4095,#4096));
#796=EDGE_LOOP('',(#4097,#4098,#4099,#4100));
#797=EDGE_LOOP('',(#4101,#4102,#4103,#4104));
#798=EDGE_LOOP('',(#4105,#4106,#4107,#4108));
#799=EDGE_LOOP('',(#4109,#4110,#4111,#4112));
#800=EDGE_LOOP('',(#4113,#4114,#4115,#4116));
#801=EDGE_LOOP('',(#4117,#4118,#4119,#4120));
#802=EDGE_LOOP('',(#4121));
#803=EDGE_LOOP('',(#4122,#4123,#4124,#4125,#4126,#4127));
#804=EDGE_LOOP('',(#4128,#4129,#4130,#4131));
#805=EDGE_LOOP('',(#4132));
#1166=LINE('',#19467,#1522);
#1167=LINE('',#19478,#1523);
#1168=LINE('',#19480,#1524);
#1169=LINE('',#19484,#1525);
#1170=LINE('',#19486,#1526);
#1171=LINE('',#19487,#1527);
#1172=LINE('',#19490,#1528);
#1173=LINE('',#19491,#1529);
#1174=LINE('',#19494,#1530);
#1175=LINE('',#19495,#1531);
#1176=LINE('',#19498,#1532);
#1177=LINE('',#19499,#1533);
#1178=LINE('',#19502,#1534);
#1179=LINE('',#19503,#1535);
#1180=LINE('',#19505,#1536);
#1181=LINE('',#19509,#1537);
#1182=LINE('',#19510,#1538);
#1183=LINE('',#19511,#1539);
#1184=LINE('',#19514,#1540);
#1185=LINE('',#19515,#1541);
#1186=LINE('',#19518,#1542);
#1187=LINE('',#19519,#1543);
#1188=LINE('',#19522,#1544);
#1189=LINE('',#19523,#1545);
#1190=LINE('',#19526,#1546);
#1191=LINE('',#19527,#1547);
#1192=LINE('',#19529,#1548);
#1193=LINE('',#19534,#1549);
#1522=VECTOR('',#6330,7.28);
#1523=VECTOR('',#6345,11.24);
#1524=VECTOR('',#6348,7.911);
#1525=VECTOR('',#6351,10.);
#1526=VECTOR('',#6352,10.);
#1527=VECTOR('',#6353,10.);
#1528=VECTOR('',#6356,10.);
#1529=VECTOR('',#6357,10.);
#1530=VECTOR('',#6360,10.);
#1531=VECTOR('',#6361,10.);
#1532=VECTOR('',#6364,9.99999999999999);
#1533=VECTOR('',#6365,10.);
#1534=VECTOR('',#6368,10.);
#1535=VECTOR('',#6369,10.);
#1536=VECTOR('',#6372,10.);
#1537=VECTOR('',#6375,10.);
#1538=VECTOR('',#6376,10.);
#1539=VECTOR('',#6377,10.);
#1540=VECTOR('',#6380,10.);
#1541=VECTOR('',#6381,10.);
#1542=VECTOR('',#6384,10.);
#1543=VECTOR('',#6385,10.);
#1544=VECTOR('',#6388,9.99999999999999);
#1545=VECTOR('',#6389,10.);
#1546=VECTOR('',#6392,10.);
#1547=VECTOR('',#6393,10.);
#1548=VECTOR('',#6396,10.);
#1549=VECTOR('',#6403,14.48);
#1778=CIRCLE('',#5226,7.911);
#1779=CIRCLE('',#5227,6.4);
#1780=CIRCLE('',#5229,7.911);
#1781=CIRCLE('',#5230,1.);
#1782=CIRCLE('',#5231,8.20389321881349);
#1783=CIRCLE('',#5233,14.48);
#1784=CIRCLE('',#5248,14.48);
#2216=VERTEX_POINT('',#19464);
#2217=VERTEX_POINT('',#19466);
#2218=VERTEX_POINT('',#19470);
#2219=VERTEX_POINT('',#19472);
#2220=VERTEX_POINT('',#19476);
#2221=VERTEX_POINT('',#19482);
#2222=VERTEX_POINT('',#19483);
#2223=VERTEX_POINT('',#19485);
#2224=VERTEX_POINT('',#19489);
#2225=VERTEX_POINT('',#19493);
#2226=VERTEX_POINT('',#19497);
#2227=VERTEX_POINT('',#19501);
#2228=VERTEX_POINT('',#19507);
#2229=VERTEX_POINT('',#19508);
#2230=VERTEX_POINT('',#19513);
#2231=VERTEX_POINT('',#19517);
#2232=VERTEX_POINT('',#19521);
#2233=VERTEX_POINT('',#19525);
#2234=VERTEX_POINT('',#19531);
#2843=EDGE_CURVE('',#2216,#2216,#1778,.T.);
#2844=EDGE_CURVE('',#2216,#2217,#1166,.T.);
#2845=EDGE_CURVE('',#2217,#2217,#1779,.T.);
#2846=EDGE_CURVE('',#2218,#2218,#1780,.T.);
#2847=EDGE_CURVE('',#2218,#2219,#1781,.T.);
#2848=EDGE_CURVE('',#2219,#2219,#1782,.T.);
#2849=EDGE_CURVE('',#2220,#2220,#1783,.T.);
#2850=EDGE_CURVE('',#2220,#2219,#1167,.T.);
#2851=EDGE_CURVE('',#2216,#2218,#1168,.T.);
#2852=EDGE_CURVE('',#2221,#2222,#1169,.T.);
#2853=EDGE_CURVE('',#2223,#2221,#1170,.T.);
#2854=EDGE_CURVE('',#2223,#2222,#1171,.T.);
#2855=EDGE_CURVE('',#2224,#2223,#1172,.T.);
#2856=EDGE_CURVE('',#2224,#2222,#1173,.T.);
#2857=EDGE_CURVE('',#2225,#2224,#1174,.T.);
#2858=EDGE_CURVE('',#2225,#2222,#1175,.T.);
#2859=EDGE_CURVE('',#2226,#2225,#1176,.T.);
#2860=EDGE_CURVE('',#2226,#2222,#1177,.T.);
#2861=EDGE_CURVE('',#2227,#2226,#1178,.T.);
#2862=EDGE_CURVE('',#2227,#2222,#1179,.T.);
#2863=EDGE_CURVE('',#2221,#2227,#1180,.T.);
#2864=EDGE_CURVE('',#2228,#2229,#1181,.T.);
#2865=EDGE_CURVE('',#2228,#2223,#1182,.T.);
#2866=EDGE_CURVE('',#2229,#2221,#1183,.T.);
#2867=EDGE_CURVE('',#2230,#2228,#1184,.T.);
#2868=EDGE_CURVE('',#2230,#2224,#1185,.T.);
#2869=EDGE_CURVE('',#2231,#2230,#1186,.T.);
#2870=EDGE_CURVE('',#2231,#2225,#1187,.T.);
#2871=EDGE_CURVE('',#2232,#2231,#1188,.T.);
#2872=EDGE_CURVE('',#2232,#2226,#1189,.T.);
#2873=EDGE_CURVE('',#2233,#2232,#1190,.T.);
#2874=EDGE_CURVE('',#2233,#2227,#1191,.T.);
#2875=EDGE_CURVE('',#2229,#2233,#1192,.T.);
#2876=EDGE_CURVE('',#2234,#2234,#1784,.T.);
#2877=EDGE_CURVE('',#2220,#2234,#1193,.T.);
#4063=ORIENTED_EDGE('',*,*,#2843,.F.);
#4064=ORIENTED_EDGE('',*,*,#2844,.T.);
#4065=ORIENTED_EDGE('',*,*,#2845,.F.);
#4066=ORIENTED_EDGE('',*,*,#2844,.F.);
#4067=ORIENTED_EDGE('',*,*,#2846,.T.);
#4068=ORIENTED_EDGE('',*,*,#2847,.T.);
#4069=ORIENTED_EDGE('',*,*,#2848,.T.);
#4070=ORIENTED_EDGE('',*,*,#2847,.F.);
#4071=ORIENTED_EDGE('',*,*,#2849,.T.);
#4072=ORIENTED_EDGE('',*,*,#2850,.T.);
#4073=ORIENTED_EDGE('',*,*,#2848,.F.);
#4074=ORIENTED_EDGE('',*,*,#2850,.F.);
#4075=ORIENTED_EDGE('',*,*,#2843,.T.);
#4076=ORIENTED_EDGE('',*,*,#2851,.T.);
#4077=ORIENTED_EDGE('',*,*,#2846,.F.);
#4078=ORIENTED_EDGE('',*,*,#2851,.F.);
#4079=ORIENTED_EDGE('',*,*,#2852,.F.);
#4080=ORIENTED_EDGE('',*,*,#2853,.F.);
#4081=ORIENTED_EDGE('',*,*,#2854,.T.);
#4082=ORIENTED_EDGE('',*,*,#2854,.F.);
#4083=ORIENTED_EDGE('',*,*,#2855,.F.);
#4084=ORIENTED_EDGE('',*,*,#2856,.T.);
#4085=ORIENTED_EDGE('',*,*,#2856,.F.);
#4086=ORIENTED_EDGE('',*,*,#2857,.F.);
#4087=ORIENTED_EDGE('',*,*,#2858,.T.);
#4088=ORIENTED_EDGE('',*,*,#2858,.F.);
#4089=ORIENTED_EDGE('',*,*,#2859,.F.);
#4090=ORIENTED_EDGE('',*,*,#2860,.T.);
#4091=ORIENTED_EDGE('',*,*,#2860,.F.);
#4092=ORIENTED_EDGE('',*,*,#2861,.F.);
#4093=ORIENTED_EDGE('',*,*,#2862,.T.);
#4094=ORIENTED_EDGE('',*,*,#2862,.F.);
#4095=ORIENTED_EDGE('',*,*,#2863,.F.);
#4096=ORIENTED_EDGE('',*,*,#2852,.T.);
#4097=ORIENTED_EDGE('',*,*,#2864,.F.);
#4098=ORIENTED_EDGE('',*,*,#2865,.T.);
#4099=ORIENTED_EDGE('',*,*,#2853,.T.);
#4100=ORIENTED_EDGE('',*,*,#2866,.F.);
#4101=ORIENTED_EDGE('',*,*,#2867,.F.);
#4102=ORIENTED_EDGE('',*,*,#2868,.T.);
#4103=ORIENTED_EDGE('',*,*,#2855,.T.);
#4104=ORIENTED_EDGE('',*,*,#2865,.F.);
#4105=ORIENTED_EDGE('',*,*,#2869,.F.);
#4106=ORIENTED_EDGE('',*,*,#2870,.T.);
#4107=ORIENTED_EDGE('',*,*,#2857,.T.);
#4108=ORIENTED_EDGE('',*,*,#2868,.F.);
#4109=ORIENTED_EDGE('',*,*,#2871,.F.);
#4110=ORIENTED_EDGE('',*,*,#2872,.T.);
#4111=ORIENTED_EDGE('',*,*,#2859,.T.);
#4112=ORIENTED_EDGE('',*,*,#2870,.F.);
#4113=ORIENTED_EDGE('',*,*,#2873,.F.);
#4114=ORIENTED_EDGE('',*,*,#2874,.T.);
#4115=ORIENTED_EDGE('',*,*,#2861,.T.);
#4116=ORIENTED_EDGE('',*,*,#2872,.F.);
#4117=ORIENTED_EDGE('',*,*,#2875,.F.);
#4118=ORIENTED_EDGE('',*,*,#2866,.T.);
#4119=ORIENTED_EDGE('',*,*,#2863,.T.);
#4120=ORIENTED_EDGE('',*,*,#2874,.F.);
#4121=ORIENTED_EDGE('',*,*,#2876,.F.);
#4122=ORIENTED_EDGE('',*,*,#2864,.T.);
#4123=ORIENTED_EDGE('',*,*,#2875,.T.);
#4124=ORIENTED_EDGE('',*,*,#2873,.T.);
#4125=ORIENTED_EDGE('',*,*,#2871,.T.);
#4126=ORIENTED_EDGE('',*,*,#2869,.T.);
#4127=ORIENTED_EDGE('',*,*,#2867,.T.);
#4128=ORIENTED_EDGE('',*,*,#2849,.F.);
#4129=ORIENTED_EDGE('',*,*,#2877,.T.);
#4130=ORIENTED_EDGE('',*,*,#2876,.T.);
#4131=ORIENTED_EDGE('',*,*,#2877,.F.);
#4132=ORIENTED_EDGE('',*,*,#2845,.T.);
#4514=CYLINDRICAL_SURFACE('',#5234,7.911);
#4515=CYLINDRICAL_SURFACE('',#5249,14.48);
#4731=ADVANCED_FACE('',(#507),#59,.T.);
#4732=ADVANCED_FACE('',(#508),#44,.F.);
#4733=ADVANCED_FACE('',(#509),#60,.T.);
#4734=ADVANCED_FACE('',(#510),#4514,.T.);
#4735=ADVANCED_FACE('',(#511),#287,.F.);
#4736=ADVANCED_FACE('',(#512),#288,.F.);
#4737=ADVANCED_FACE('',(#513),#289,.F.);
#4738=ADVANCED_FACE('',(#514),#290,.F.);
#4739=ADVANCED_FACE('',(#515),#291,.F.);
#4740=ADVANCED_FACE('',(#516),#292,.F.);
#4741=ADVANCED_FACE('',(#517),#293,.F.);
#4742=ADVANCED_FACE('',(#518),#294,.F.);
#4743=ADVANCED_FACE('',(#519),#295,.F.);
#4744=ADVANCED_FACE('',(#520),#296,.F.);
#4745=ADVANCED_FACE('',(#521),#297,.F.);
#4746=ADVANCED_FACE('',(#522),#298,.F.);
#4747=ADVANCED_FACE('',(#523,#94),#299,.T.);
#4748=ADVANCED_FACE('',(#524),#4515,.T.);
#4749=ADVANCED_FACE('',(#525),#300,.T.);
#4827=CLOSED_SHELL('',(#4731,#4732,#4733,#4734,#4735,#4736,#4737,#4738,
#4739,#4740,#4741,#4742,#4743,#4744,#4745,#4746,#4747,#4748,#4749));
#5224=AXIS2_PLACEMENT_3D('',#19462,#6324,#6325);
#5225=AXIS2_PLACEMENT_3D('',#19463,#6326,#6327);
#5226=AXIS2_PLACEMENT_3D('',#19465,#6328,#6329);
#5227=AXIS2_PLACEMENT_3D('',#19468,#6331,#6332);
#5228=AXIS2_PLACEMENT_3D('',#19469,#6333,#6334);
#5229=AXIS2_PLACEMENT_3D('',#19471,#6335,#6336);
#5230=AXIS2_PLACEMENT_3D('',#19473,#6337,#6338);
#5231=AXIS2_PLACEMENT_3D('',#19474,#6339,#6340);
#5232=AXIS2_PLACEMENT_3D('',#19475,#6341,#6342);
#5233=AXIS2_PLACEMENT_3D('',#19477,#6343,#6344);
#5234=AXIS2_PLACEMENT_3D('',#19479,#6346,#6347);
#5235=AXIS2_PLACEMENT_3D('',#19481,#6349,#6350);
#5236=AXIS2_PLACEMENT_3D('',#19488,#6354,#6355);
#5237=AXIS2_PLACEMENT_3D('',#19492,#6358,#6359);
#5238=AXIS2_PLACEMENT_3D('',#19496,#6362,#6363);
#5239=AXIS2_PLACEMENT_3D('',#19500,#6366,#6367);
#5240=AXIS2_PLACEMENT_3D('',#19504,#6370,#6371);
#5241=AXIS2_PLACEMENT_3D('',#19506,#6373,#6374);
#5242=AXIS2_PLACEMENT_3D('',#19512,#6378,#6379);
#5243=AXIS2_PLACEMENT_3D('',#19516,#6382,#6383);
#5244=AXIS2_PLACEMENT_3D('',#19520,#6386,#6387);
#5245=AXIS2_PLACEMENT_3D('',#19524,#6390,#6391);
#5246=AXIS2_PLACEMENT_3D('',#19528,#6394,#6395);
#5247=AXIS2_PLACEMENT_3D('',#19530,#6397,#6398);
#5248=AXIS2_PLACEMENT_3D('',#19532,#6399,#6400);
#5249=AXIS2_PLACEMENT_3D('',#19533,#6401,#6402);
#5250=AXIS2_PLACEMENT_3D('',#19535,#6404,#6405);
#6324=DIRECTION('axis',(0.,0.,1.));
#6325=DIRECTION('refdir',(1.,0.,0.));
#6326=DIRECTION('center_axis',(-7.86407975776121E-17,0.,1.));
#6327=DIRECTION('ref_axis',(-1.,0.,-7.86407975776121E-17));
#6328=DIRECTION('center_axis',(-7.86407975776121E-17,0.,1.));
#6329=DIRECTION('ref_axis',(-1.,0.,-7.86407975776121E-17));
#6330=DIRECTION('',(-0.739940073395942,-9.06165242445198E-17,-0.672672793996315));
#6331=DIRECTION('center_axis',(7.86407975776121E-17,0.,-1.));
#6332=DIRECTION('ref_axis',(-1.,0.,-7.86407975776121E-17));
#6333=DIRECTION('center_axis',(7.86407975776121E-17,0.,-1.));
#6334=DIRECTION('ref_axis',(-1.,0.,-8.96154192009005E-17));
#6335=DIRECTION('center_axis',(-7.86407975776121E-17,0.,1.));
#6336=DIRECTION('ref_axis',(-1.,0.,-7.86407975776121E-17));
#6337=DIRECTION('center_axis',(1.22464679914735E-16,1.,9.63072010358176E-33));
#6338=DIRECTION('ref_axis',(1.,-1.22464679914735E-16,1.12019274001126E-16));
#6339=DIRECTION('center_axis',(0.,0.,-1.));
#6340=DIRECTION('ref_axis',(-1.,6.12323399573677E-17,0.));
#6341=DIRECTION('center_axis',(-7.86407975776121E-17,0.,1.));
#6342=DIRECTION('ref_axis',(-1.,0.,-7.86407975776121E-17));
#6343=DIRECTION('center_axis',(7.86407975776121E-17,0.,-1.));
#6344=DIRECTION('ref_axis',(1.,0.,7.86407975776121E-17));
#6345=DIRECTION('',(-0.70710678118658,-8.65956056235534E-17,-0.707106781186515));
#6346=DIRECTION('center_axis',(7.86407975776121E-17,0.,-1.));
#6347=DIRECTION('ref_axis',(-1.,0.,-7.86407975776121E-17));
#6348=DIRECTION('',(-7.86407975776121E-17,0.,1.));
#6349=DIRECTION('center_axis',(0.25,0.433012701892219,-0.866025403784439));
#6350=DIRECTION('ref_axis',(0.866025403784439,-0.5,2.49215522988657E-16));
#6351=DIRECTION('',(-0.774596669241483,-0.447213595499958,-0.447213595499958));
#6352=DIRECTION('',(0.866025403784439,-0.5,6.81049284760846E-17));
#6353=DIRECTION('',(-1.1466334093198E-16,-0.894427190999916,-0.447213595499958));
#6354=DIRECTION('center_axis',(-0.25,0.433012701892219,-0.866025403784439));
#6355=DIRECTION('ref_axis',(0.866025403784439,0.5,-1.73385880213439E-16));
#6356=DIRECTION('',(0.866025403784439,0.5,6.81049284760846E-17));
#6357=DIRECTION('',(0.774596669241484,-0.447213595499958,-0.447213595499958));
#6358=DIRECTION('center_axis',(-0.5,-1.92296268638357E-16,-0.866025403784439));
#6359=DIRECTION('ref_axis',(-3.84592537276713E-16,1.,-4.40476560101798E-31));
#6360=DIRECTION('',(-3.84592537276713E-16,1.,-3.02446638738394E-32));
#6361=DIRECTION('',(0.774596669241483,0.447213595499958,-0.447213595499958));
#6362=DIRECTION('center_axis',(-0.25,-0.433012701892219,-0.866025403784439));
#6363=DIRECTION('ref_axis',(-0.866025403784438,0.5,-2.09031490959634E-17));
#6364=DIRECTION('',(-0.866025403784438,0.5,-6.81049284760846E-17));
#6365=DIRECTION('',(6.87980045591882E-16,0.894427190999916,-0.447213595499958));
#6366=DIRECTION('center_axis',(0.25,-0.43301270189222,-0.866025403784438));
#6367=DIRECTION('ref_axis',(-0.866025403784439,-0.499999999999999,-1.78830203614062E-16));
#6368=DIRECTION('',(-0.866025403784439,-0.499999999999999,-6.81049284760846E-17));
#6369=DIRECTION('',(-0.774596669241483,0.447213595499959,-0.447213595499958));
#6370=DIRECTION('center_axis',(0.5,0.,-0.866025403784438));
#6371=DIRECTION('ref_axis',(0.,-1.,0.));
#6372=DIRECTION('',(0.,-1.,0.));
#6373=DIRECTION('center_axis',(0.5,0.866025403784439,5.78241158658936E-17));
#6374=DIRECTION('ref_axis',(0.866025403784439,-0.5,6.81049284760846E-17));
#6375=DIRECTION('',(0.866025403784439,-0.5,6.81049284760818E-17));
#6376=DIRECTION('',(1.15648231731787E-16,0.,-1.));
#6377=DIRECTION('',(1.15648231731787E-16,0.,-1.));
#6378=DIRECTION('center_axis',(-0.5,0.866025403784439,-5.78241158658936E-17));
#6379=DIRECTION('ref_axis',(0.866025403784439,0.5,6.81049284760846E-17));
#6380=DIRECTION('',(0.866025403784439,0.5,6.81049284760818E-17));
#6381=DIRECTION('',(1.15648231731787E-16,0.,-1.));
#6382=DIRECTION('center_axis',(-1.,-3.84592537276713E-16,-1.15648231731787E-16));
#6383=DIRECTION('ref_axis',(-3.84592537276713E-16,1.,-3.02446638738394E-32));
#6384=DIRECTION('',(-3.84592537276713E-16,1.,-3.02446638738382E-32));
#6385=DIRECTION('',(1.15648231731787E-16,0.,-1.));
#6386=DIRECTION('center_axis',(-0.5,-0.866025403784439,-5.78241158658936E-17));
#6387=DIRECTION('ref_axis',(-0.866025403784439,0.5,-6.81049284760847E-17));
#6388=DIRECTION('',(-0.866025403784438,0.5,-6.81049284760818E-17));
#6389=DIRECTION('',(1.15648231731787E-16,0.,-1.));
#6390=DIRECTION('center_axis',(0.499999999999999,-0.866025403784439,5.78241158658935E-17));
#6391=DIRECTION('ref_axis',(-0.866025403784439,-0.499999999999999,-6.81049284760846E-17));
#6392=DIRECTION('',(-0.866025403784439,-0.499999999999999,-6.81049284760819E-17));
#6393=DIRECTION('',(1.15648231731787E-16,0.,-1.));
#6394=DIRECTION('center_axis',(1.,0.,1.15648231731787E-16));
#6395=DIRECTION('ref_axis',(0.,-1.,0.));
#6396=DIRECTION('',(0.,-1.,0.));
#6397=DIRECTION('center_axis',(-7.86407975776121E-17,0.,1.));
#6398=DIRECTION('ref_axis',(1.,0.,7.86407975776121E-17));
#6399=DIRECTION('center_axis',(7.86407975776121E-17,0.,-1.));
#6400=DIRECTION('ref_axis',(1.,0.,7.86407975776121E-17));
#6401=DIRECTION('center_axis',(7.86407975776121E-17,0.,-1.));
#6402=DIRECTION('ref_axis',(-1.,0.,-7.86407975776121E-17));
#6403=DIRECTION('',(-7.86407975776121E-17,0.,1.));
#6404=DIRECTION('center_axis',(7.86407975776121E-17,0.,-1.));
#6405=DIRECTION('ref_axis',(-1.,0.,-7.86407975776121E-17));
#19462=CARTESIAN_POINT('',(0.,0.,0.));
#19463=CARTESIAN_POINT('Origin',(-8.50613908013701E-14,0.,-14.2400000000013));
#19464=CARTESIAN_POINT('',(7.91099999999991,9.68818082805471E-16,-13.6663636363649));
#19465=CARTESIAN_POINT('Origin',(-8.5106502022526E-14,0.,-13.6663636363649));
#19466=CARTESIAN_POINT('',(6.39999999999992,-7.83773951454306E-16,-15.0400000000013));
#19467=CARTESIAN_POINT('',(7.27999999999992,8.91542869779273E-16,-14.2400000000013));
#19468=CARTESIAN_POINT('Origin',(-8.4998478163308E-14,0.,-15.0400000000013));
#19469=CARTESIAN_POINT('Origin',(-8.67707890235993E-14,0.,7.49678643762621));
#19470=CARTESIAN_POINT('',(7.91099999999991,9.68818082805471E-16,7.49678643762622));
#19471=CARTESIAN_POINT('Origin',(-8.67707890235993E-14,0.,7.49678643762621));
#19472=CARTESIAN_POINT('',(8.2038932188134,-2.00937431419332E-15,8.20389321881279));
#19473=CARTESIAN_POINT('Origin',(8.91099999999991,-1.09128276272021E-15,
7.49678643762621));
#19474=CARTESIAN_POINT('Origin',(-8.54871728961371E-14,-5.02343578548331E-16,
8.20389321881279));
#19475=CARTESIAN_POINT('Origin',(-8.70651583236477E-14,0.,11.239999999999));
#19476=CARTESIAN_POINT('',(14.4799999999999,-1.77328856516537E-15,14.4799999999987));
#19477=CARTESIAN_POINT('Origin',(-8.73199545077991E-14,0.,14.4799999999987));
#19478=CARTESIAN_POINT('',(11.2399999999999,1.37650300224163E-15,11.239999999999));
#19479=CARTESIAN_POINT('Origin',(-8.59044201514021E-14,0.,-3.52000000000102));
#19480=CARTESIAN_POINT('',(7.91099999999991,-9.68818082805471E-16,-3.52000000000102));
#19481=CARTESIAN_POINT('Origin',(5.,2.88675134594813,10.1599999999987));
#19482=CARTESIAN_POINT('',(5.,2.88675134594813,10.1599999999987));
#19483=CARTESIAN_POINT('',(2.77555756156289E-15,3.60822483003176E-15,7.2732486540506));
#19484=CARTESIAN_POINT('',(3.99999999999999,2.3094010767585,9.5826497308091));
#19485=CARTESIAN_POINT('',(-5.55111512312578E-16,5.77350269189626,10.1599999999987));
#19486=CARTESIAN_POINT('',(-2.13056424354826E-15,5.77350269189626,10.1599999999987));
#19487=CARTESIAN_POINT('',(-1.66533453693773E-15,4.61880215351701,9.5826497308091));
#19488=CARTESIAN_POINT('Origin',(-5.55111512312578E-16,5.77350269189626,
10.1599999999987));
#19489=CARTESIAN_POINT('',(-5.,2.88675134594813,10.1599999999987));
#19490=CARTESIAN_POINT('',(-5.,2.88675134594813,10.1599999999987));
#19491=CARTESIAN_POINT('',(-4.,2.3094010767585,9.5826497308091));
#19492=CARTESIAN_POINT('Origin',(-5.,2.88675134594813,10.1599999999987));
#19493=CARTESIAN_POINT('',(-5.00000000000001,-2.88675134594812,10.1599999999987));
#19494=CARTESIAN_POINT('',(-5.,-2.88675134594812,10.1599999999987));
#19495=CARTESIAN_POINT('',(-4.,-2.3094010767585,9.5826497308091));
#19496=CARTESIAN_POINT('Origin',(-5.00000000000001,-2.88675134594812,10.1599999999987));
#19497=CARTESIAN_POINT('',(-1.0547118733939E-14,-5.77350269189626,10.1599999999987));
#19498=CARTESIAN_POINT('',(-6.37301395980167E-15,-5.77350269189625,10.1599999999987));
#19499=CARTESIAN_POINT('',(-4.9960036108132E-15,-4.618802153517,9.5826497308091));
#19500=CARTESIAN_POINT('Origin',(-1.0547118733939E-14,-5.77350269189626,
10.1599999999987));
#19501=CARTESIAN_POINT('',(4.99999999999999,-2.88675134594813,10.1599999999987));
#19502=CARTESIAN_POINT('',(4.99999999999999,-2.88675134594813,10.1599999999987));
#19503=CARTESIAN_POINT('',(4.,-2.3094010767585,9.5826497308091));
#19504=CARTESIAN_POINT('Origin',(4.99999999999999,-2.88675134594813,10.1599999999987));
#19505=CARTESIAN_POINT('',(5.,2.88675134594813,10.1599999999987));
#19506=CARTESIAN_POINT('Origin',(-2.03450935938186E-15,5.77350269189626,
14.9599999999987));
#19507=CARTESIAN_POINT('',(-1.17646633176102E-15,5.77350269189626,14.9599999999987));
#19508=CARTESIAN_POINT('',(5.,2.88675134594813,14.9599999999987));
#19509=CARTESIAN_POINT('',(-4.18000000000003,8.18682681710891,14.9599999999987));
#19510=CARTESIAN_POINT('',(-1.17646633176102E-15,5.77350269189626,14.9599999999987));
#19511=CARTESIAN_POINT('',(5.,2.88675134594813,14.9599999999987));
#19512=CARTESIAN_POINT('Origin',(-5.,2.88675134594813,14.9599999999987));
#19513=CARTESIAN_POINT('',(-5.00000000000001,2.88675134594813,14.9599999999987));
#19514=CARTESIAN_POINT('',(-9.18000000000004,0.473427220735475,14.9599999999987));
#19515=CARTESIAN_POINT('',(-5.00000000000001,2.88675134594813,14.9599999999987));
#19516=CARTESIAN_POINT('Origin',(-5.,-2.88675134594812,14.9599999999987));
#19517=CARTESIAN_POINT('',(-5.00000000000001,-2.88675134594812,14.9599999999987));
#19518=CARTESIAN_POINT('',(-5.,-1.44337567297406,14.9599999999987));
#19519=CARTESIAN_POINT('',(-5.00000000000001,-2.88675134594812,14.9599999999987));
#19520=CARTESIAN_POINT('Origin',(-9.14690518987735E-15,-5.77350269189625,
14.9599999999987));
#19521=CARTESIAN_POINT('',(-1.11684735533874E-14,-5.77350269189626,14.9599999999987));
#19522=CARTESIAN_POINT('',(-6.68000000000004,-1.91680289370953,14.9599999999987));
#19523=CARTESIAN_POINT('',(-1.11684735533874E-14,-5.77350269189626,14.9599999999987));
#19524=CARTESIAN_POINT('Origin',(4.99999999999999,-2.88675134594813,14.9599999999987));
#19525=CARTESIAN_POINT('',(4.99999999999999,-2.88675134594813,14.9599999999987));
#19526=CARTESIAN_POINT('',(-1.68000000000005,-6.74345114413485,14.9599999999987));
#19527=CARTESIAN_POINT('',(4.99999999999999,-2.88675134594813,14.9599999999987));
#19528=CARTESIAN_POINT('Origin',(5.,2.88675134594813,14.9599999999987));
#19529=CARTESIAN_POINT('',(5.,1.44337567297406,14.9599999999987));
#19530=CARTESIAN_POINT('Origin',(-14.4800000000001,0.,14.9599999999987));
#19531=CARTESIAN_POINT('',(14.4799999999999,-1.77328856516537E-15,14.9599999999987));
#19532=CARTESIAN_POINT('Origin',(-8.73577020906364E-14,0.,14.9599999999987));
#19533=CARTESIAN_POINT('Origin',(-8.73388282992177E-14,0.,14.7199999999987));
#19534=CARTESIAN_POINT('',(14.4799999999999,-1.77328856516537E-15,14.7199999999987));
#19535=CARTESIAN_POINT('Origin',(-8.54871728961371E-14,0.,-15.0400000000013));
#19864=UNCERTAINTY_MEASURE_WITH_UNIT(LENGTH_MEASURE(0.01),#19879,
'DISTANCE_ACCURACY_VALUE',
'Maximum model space distance between geometric entities at asserted c
onnectivities');
#19869=UNCERTAINTY_MEASURE_WITH_UNIT(LENGTH_MEASURE(0.01),#19879,
'DISTANCE_ACCURACY_VALUE',
'Maximum model space distance between geometric entities at asserted c
onnectivities');
#19873=(
GEOMETRIC_REPRESENTATION_CONTEXT(3)
GLOBAL_UNCERTAINTY_ASSIGNED_CONTEXT((#19864))
GLOBAL_UNIT_ASSIGNED_CONTEXT((#19879,#19881,#19882))
REPRESENTATION_CONTEXT('','3D')
);
#19878=(
GEOMETRIC_REPRESENTATION_CONTEXT(3)
GLOBAL_UNCERTAINTY_ASSIGNED_CONTEXT((#19869))
GLOBAL_UNIT_ASSIGNED_CONTEXT((#19879,#19881,#19882))
REPRESENTATION_CONTEXT('','3D')
);
#19879=(
LENGTH_UNIT()
NAMED_UNIT(*)
SI_UNIT(.MILLI.,.METRE.)
);
#19881=(
NAMED_UNIT(*)
PLANE_ANGLE_UNIT()
SI_UNIT($,.RADIAN.)
);
#19882=(
NAMED_UNIT(*)
SI_UNIT($,.STERADIAN.)
SOLID_ANGLE_UNIT()
);
#19886=SHAPE_DEFINITION_REPRESENTATION(#19894,#19909);
#19894=PRODUCT_DEFINITION_SHAPE('',$,#19918);
#19909=SHAPE_REPRESENTATION('',(#5224),#19873);
#19914=PRODUCT_DEFINITION_CONTEXT('part definition',#19940,'design');
#19918=PRODUCT_DEFINITION(
'BHSFCHCS ANSI B18.3.5M - M16x30 Steel Grade 2 Plain_1','Screw_01',#19926,
#19914);
#19926=PRODUCT_DEFINITION_FORMATION('',$,#19945);
#19940=APPLICATION_CONTEXT(
'Core Data for Automotive Mechanical Design Process');
#19941=PRODUCT_CONTEXT('part definition',#19940,'mechanical');
#19945=PRODUCT('BHSFCHCS ANSI B18.3.5M - M16x30 Steel Grade 2 Plain_1',
'Screw_01',
'Broached Hexagon Socket Flat Countersunk Head Cap Screw ANSI B18.3.5M
 - M16x30',(#19941));
#19952=PRESENTATION_STYLE_ASSIGNMENT((#19958));
#19958=SURFACE_STYLE_USAGE(.BOTH.,#19964);
#19964=SURFACE_SIDE_STYLE('',(#19970));
#19970=SURFACE_STYLE_FILL_AREA(#19976);
#19976=FILL_AREA_STYLE('Opaque(160,160,160)',(#19982));
#19982=FILL_AREA_STYLE_COLOUR('Opaque(160,160,160)',#19988);
#19988=COLOUR_RGB('Opaque(160,160,160)', 0.66274510, 0.83137255, 0.94901961);
ENDSEC;
END-ISO-10303-21;
